ISO-10303-21;
HEADER;
FILE_DESCRIPTION (('STEP AP214'),
    '1' );
FILE_NAME ('Part13^Assem2.step',
    '2026-11-01T06:29:40',
    ( '' ),
    ( '' ),
    'SwSTEP 2.0',
    'SolidWorks 2024',
    '' );
FILE_SCHEMA (( 'AUTOMOTIVE_DESIGN' ));
ENDSEC;

DATA;
#97=MECHANICAL_DESIGN_GEOMETRIC_PRESENTATION_REPRESENTATION('',(#748),#10965);
#121=PRESENTATION_STYLE_ASSIGNMENT (( #11153 ) ) ;
#245=ORIENTED_EDGE ( 'NONE', *, *, #2016, .F. ) ;
#406=PRESENTATION_STYLE_ASSIGNMENT (( #19728 ) ) ;
#481=AXIS2_PLACEMENT_3D ( 'NONE', #4264, #1133, #15084 ) ;
#504=VERTEX_POINT ( 'NONE', #11439 ) ;
#520=DIRECTION ( 'NONE',  ( 1.000000000000000000, 0.000000000000000000, 0.000000000000000000 ) ) ;
#748=STYLED_ITEM ( 'NONE', ( #406 ), #18434 ) ;
#916=CARTESIAN_POINT ( 'NONE',  ( -36.00000000000000000, 4.408728476930470856E-15, 0.000000000000000000 ) ) ;
#1133=DIRECTION ( 'NONE',  ( 0.000000000000000000, 0.000000000000000000, 1.000000000000000000 ) ) ;
#1140=DIRECTION ( 'NONE',  ( 0.000000000000000000, 0.000000000000000000, 1.000000000000000000 ) ) ;
#1450=STYLED_ITEM ( 'NONE', ( #121 ), #15204 ) ;
#1553=DIRECTION ( 'NONE',  ( 0.000000000000000000, 0.000000000000000000, 1.000000000000000000 ) ) ;
#1678=CYLINDRICAL_SURFACE ( 'NONE', #10364, 36.00000000000000000 ) ;
#1920=ORIENTED_EDGE ( 'NONE', *, *, #16701, .T. ) ;
#1940=CARTESIAN_POINT ( 'NONE',  ( 0.000000000000000000, 0.000000000000000000, 0.000000000000000000 ) ) ;
#1944=SURFACE_STYLE_FILL_AREA ( #3622 ) ;
#2016=EDGE_CURVE ( 'NONE', #11845, #5865, #11686, .T. ) ;
#2097=LINE ( 'NONE', #6872, #15669 ) ;
#2413=( GEOMETRIC_REPRESENTATION_CONTEXT ( 3 ) GLOBAL_UNCERTAINTY_ASSIGNED_CONTEXT ( ( #2650 ) ) GLOBAL_UNIT_ASSIGNED_CONTEXT ( ( #6675, #14587, #17984 ) ) REPRESENTATION_CONTEXT ( 'NONE', 'WORKASPACE' ) );
#2477=STYLED_ITEM ( 'NONE', ( #9438 ), #14410 ) ;
#2482=VERTEX_POINT ( 'NONE', #916 ) ;
#2521=SHAPE_DEFINITION_REPRESENTATION ( #4647, #11716 ) ;
#2650=UNCERTAINTY_MEASURE_WITH_UNIT (LENGTH_MEASURE( 1.000000000000000082E-05 ), #6675, 'distance_accuracy_value', 'NONE');
#2741=AXIS2_PLACEMENT_3D ( 'NONE', #5042, #3500, #8234 ) ;
#2820=PRODUCT_CONTEXT ( 'NONE', #3930, 'mechanical' ) ;
#2847=DIRECTION ( 'NONE',  ( 1.000000000000000000, 0.000000000000000000, 0.000000000000000000 ) ) ;
#2871=APPLICATION_CONTEXT ( 'automotive_design' ) ;
#3008=SURFACE_SIDE_STYLE ('',( #3320 ) ) ;
#3225=( NAMED_UNIT ( * ) SI_UNIT ( $, .STERADIAN. ) SOLID_ANGLE_UNIT ( ) );
#3252=SURFACE_STYLE_USAGE ( .BOTH. , #3471 ) ;
#3320=SURFACE_STYLE_FILL_AREA ( #18870 ) ;
#3389=DIRECTION ( 'NONE',  ( 0.000000000000000000, 0.000000000000000000, 1.000000000000000000 ) ) ;
#3471=SURFACE_SIDE_STYLE ('',( #7991 ) ) ;
#3500=DIRECTION ( 'NONE',  ( 0.000000000000000000, 0.000000000000000000, 1.000000000000000000 ) ) ;
#3562=ORIENTED_EDGE ( 'NONE', *, *, #13673, .F. ) ;
#3620=SURFACE_SIDE_STYLE ('',( #13015 ) ) ;
#3622=FILL_AREA_STYLE ('',( #11450 ) ) ;
#3729=UNCERTAINTY_MEASURE_WITH_UNIT (LENGTH_MEASURE( 1.000000000000000082E-05 ), #17342, 'distance_accuracy_value', 'NONE');
#3794=STYLED_ITEM ( 'NONE', ( #9415 ), #12872 ) ;
#3796=COLOUR_RGB ( '', 0.72549020, 0.75294118, 0.79215686) ;
#3905=PRODUCT_DEFINITION_CONTEXT ( 'detailed design', #2871, 'design' ) ;
#3930=APPLICATION_CONTEXT ( 'automotive_design' ) ;
#4121=COLOUR_RGB ( '', 0.40784314, 0.44705882, 0.49803922) ;
#4197=CARTESIAN_POINT ( 'NONE',  ( 0.000000000000000000, 0.000000000000000000, -135.0000000000000284 ) ) ;
#4264=CARTESIAN_POINT ( 'NONE',  ( 0.000000000000000000, 0.000000000000000000, 0.000000000000000000 ) ) ;
#4364=SURFACE_STYLE_FILL_AREA ( #18470 ) ;
#4383=AXIS2_PLACEMENT_3D ( 'NONE', #14531, #10273, #520 ) ;
#4439=AXIS2_PLACEMENT_3D ( 'NONE', #4197, #19928, #12115 ) ;
#4478=FACE_OUTER_BOUND ( 'NONE', #16384, .T. ) ;
#4647=PRODUCT_DEFINITION_SHAPE ( 'NONE', 'NONE',  #13881 ) ;
#4670=SURFACE_STYLE_USAGE ( .BOTH. , #16848 ) ;
#4787=FILL_AREA_STYLE_COLOUR ( '', #4121 ) ;
#4903=( NAMED_UNIT ( * ) PLANE_ANGLE_UNIT ( ) SI_UNIT ( $, .RADIAN. ) );
#4911=DIRECTION ( 'NONE',  ( 1.000000000000000000, 0.000000000000000000, 0.000000000000000000 ) ) ;
#5042=CARTESIAN_POINT ( 'NONE',  ( 0.000000000000000000, 0.000000000000000000, 0.000000000000000000 ) ) ;
#5172=PRODUCT ( 'Part13^Assem2', 'Part13^Assem2', '', ( #2820 ) ) ;
#5185=UNCERTAINTY_MEASURE_WITH_UNIT (LENGTH_MEASURE( 1.000000000000000082E-05 ), #6722, 'distance_accuracy_value', 'NONE');
#5269=SURFACE_STYLE_USAGE ( .BOTH. , #3620 ) ;
#5355=ORIENTED_EDGE ( 'NONE', *, *, #10277, .T. ) ;
#5385=UNCERTAINTY_MEASURE_WITH_UNIT (LENGTH_MEASURE( 1.000000000000000082E-05 ), #10755, 'distance_accuracy_value', 'NONE');
#5752=( GEOMETRIC_REPRESENTATION_CONTEXT ( 3 ) GLOBAL_UNCERTAINTY_ASSIGNED_CONTEXT ( ( #5185 ) ) GLOBAL_UNIT_ASSIGNED_CONTEXT ( ( #6722, #8359, #16019 ) ) REPRESENTATION_CONTEXT ( 'NONE', 'WORKASPACE' ) );
#5865=VERTEX_POINT ( 'NONE', #8894 ) ;
#6077=COLOUR_RGB ( '', 0.31764706, 0.68627451, 0.89019608) ;
#6328=( NAMED_UNIT ( * ) PLANE_ANGLE_UNIT ( ) SI_UNIT ( $, .RADIAN. ) );
#6353=AXIS2_PLACEMENT_3D ( 'NONE', #11191, #12442, #2847 ) ;
#6355=FACE_OUTER_BOUND ( 'NONE', #16752, .T. ) ;
#6675=( LENGTH_UNIT ( ) NAMED_UNIT ( * ) SI_UNIT ( .MILLI., .METRE. ) );
#6722=( LENGTH_UNIT ( ) NAMED_UNIT ( * ) SI_UNIT ( .MILLI., .METRE. ) );
#6872=CARTESIAN_POINT ( 'NONE',  ( -36.00000000000000000, 4.408728476930470856E-15, -135.0000000000000284 ) ) ;
#7103=( GEOMETRIC_REPRESENTATION_CONTEXT ( 3 ) GLOBAL_UNCERTAINTY_ASSIGNED_CONTEXT ( ( #17945 ) ) GLOBAL_UNIT_ASSIGNED_CONTEXT ( ( #7797, #4903, #15952 ) ) REPRESENTATION_CONTEXT ( 'NONE', 'WORKASPACE' ) );
#7172=DIRECTION ( 'NONE',  ( 1.000000000000000000, 0.000000000000000000, -0.000000000000000000 ) ) ;
#7476=DIRECTION ( 'NONE',  ( 1.000000000000000000, 0.000000000000000000, -0.000000000000000000 ) ) ;
#7652=ORIENTED_EDGE ( 'NONE', *, *, #14573, .F. ) ;
#7797=( LENGTH_UNIT ( ) NAMED_UNIT ( * ) SI_UNIT ( .MILLI., .METRE. ) );
#7991=SURFACE_STYLE_FILL_AREA ( #8205 ) ;
#8017=CLOSED_SHELL ( 'NONE', ( #14410, #18434, #12872, #15094 ) ) ;
#8106=CARTESIAN_POINT ( 'NONE',  ( 0.000000000000000000, 0.000000000000000000, -135.0000000000000284 ) ) ;
#8205=FILL_AREA_STYLE ('',( #12958 ) ) ;
#8234=DIRECTION ( 'NONE',  ( 1.000000000000000000, 0.000000000000000000, 0.000000000000000000 ) ) ;
#8256=PRESENTATION_STYLE_ASSIGNMENT (( #5269 ) ) ;
#8257=SURFACE_SIDE_STYLE ('',( #1944 ) ) ;
#8359=( NAMED_UNIT ( * ) PLANE_ANGLE_UNIT ( ) SI_UNIT ( $, .RADIAN. ) );
#8894=CARTESIAN_POINT ( 'NONE',  ( -36.00000000000000000, 4.408728476930470856E-15, -135.0000000000000284 ) ) ;
#9026=CIRCLE ( 'NONE', #481, 36.00000000000000000 ) ;
#9110=DIRECTION ( 'NONE',  ( 0.000000000000000000, 0.000000000000000000, 1.000000000000000000 ) ) ;
#9112=CARTESIAN_POINT ( 'NONE',  ( 0.000000000000000000, 0.000000000000000000, -135.0000000000000284 ) ) ;
#9415=PRESENTATION_STYLE_ASSIGNMENT (( #4670 ) ) ;
#9438=PRESENTATION_STYLE_ASSIGNMENT (( #3252 ) ) ;
#9717=COLOUR_RGB ( '', 0.40784314, 0.44705882, 0.49803922) ;
#9851=SHAPE_REPRESENTATION_RELATIONSHIP ( 'NONE' , 'NONE' ,  #11716, #13561 ) ;
#9902=( NAMED_UNIT ( * ) PLANE_ANGLE_UNIT ( ) SI_UNIT ( $, .RADIAN. ) );
#10273=DIRECTION ( 'NONE',  ( 0.000000000000000000, 0.000000000000000000, 1.000000000000000000 ) ) ;
#10277=EDGE_CURVE ( 'NONE', #504, #2482, #9026, .T. ) ;
#10299=AXIS2_PLACEMENT_3D ( 'NONE', #15545, #12647, #4911 ) ;
#10364=AXIS2_PLACEMENT_3D ( 'NONE', #8106, #12635, #11183 ) ;
#10755=( LENGTH_UNIT ( ) NAMED_UNIT ( * ) SI_UNIT ( .MILLI., .METRE. ) );
#10965=( GEOMETRIC_REPRESENTATION_CONTEXT ( 3 ) GLOBAL_UNCERTAINTY_ASSIGNED_CONTEXT ( ( #12166 ) ) GLOBAL_UNIT_ASSIGNED_CONTEXT ( ( #17635, #9902, #17728 ) ) REPRESENTATION_CONTEXT ( 'NONE', 'WORKASPACE' ) );
#11006=EDGE_LOOP ( 'NONE', ( #5355, #13752 ) ) ;
#11153=SURFACE_STYLE_USAGE ( .BOTH. , #3008 ) ;
#11183=DIRECTION ( 'NONE',  ( 1.000000000000000000, 0.000000000000000000, 0.000000000000000000 ) ) ;
#11191=CARTESIAN_POINT ( 'NONE',  ( 0.000000000000000000, 0.000000000000000000, 0.000000000000000000 ) ) ;
#11195=VECTOR ( 'NONE', #3389, 1000.000000000000000 ) ;
#11209=LINE ( 'NONE', #14102, #11195 ) ;
#11277=CIRCLE ( 'NONE', #6353, 36.00000000000000000 ) ;
#11345=AXIS2_PLACEMENT_3D ( 'NONE', #9112, #1553, #7476 ) ;
#11439=CARTESIAN_POINT ( 'NONE',  ( 36.00000000000000000, 0.000000000000000000, 0.000000000000000000 ) ) ;
#11450=FILL_AREA_STYLE_COLOUR ( '', #13917 ) ;
#11547=FACE_OUTER_BOUND ( 'NONE', #17462, .T. ) ;
#11686=CIRCLE ( 'NONE', #4439, 36.00000000000000000 ) ;
#11716=SHAPE_REPRESENTATION ( 'Part13^Assem2', ( #2741 ), #2413 ) ;
#11845=VERTEX_POINT ( 'NONE', #11961 ) ;
#11961=CARTESIAN_POINT ( 'NONE',  ( 36.00000000000000000, 0.000000000000000000, -135.0000000000000284 ) ) ;
#12115=DIRECTION ( 'NONE',  ( 1.000000000000000000, 0.000000000000000000, 0.000000000000000000 ) ) ;
#12166=UNCERTAINTY_MEASURE_WITH_UNIT (LENGTH_MEASURE( 1.000000000000000082E-05 ), #17635, 'distance_accuracy_value', 'NONE');
#12442=DIRECTION ( 'NONE',  ( 0.000000000000000000, 0.000000000000000000, 1.000000000000000000 ) ) ;
#12470=ORIENTED_EDGE ( 'NONE', *, *, #10277, .F. ) ;
#12635=DIRECTION ( 'NONE',  ( 0.000000000000000000, 0.000000000000000000, 1.000000000000000000 ) ) ;
#12647=DIRECTION ( 'NONE',  ( 0.000000000000000000, 0.000000000000000000, 1.000000000000000000 ) ) ;
#12872=ADVANCED_FACE ( 'NONE', ( #4478 ), #16953, .F. ) ;
#12958=FILL_AREA_STYLE_COLOUR ( '', #9717 ) ;
#13015=SURFACE_STYLE_FILL_AREA ( #17726 ) ;
#13021=( GEOMETRIC_REPRESENTATION_CONTEXT ( 3 ) GLOBAL_UNCERTAINTY_ASSIGNED_CONTEXT ( ( #3729 ) ) GLOBAL_UNIT_ASSIGNED_CONTEXT ( ( #17342, #14139, #3225 ) ) REPRESENTATION_CONTEXT ( 'NONE', 'WORKASPACE' ) );
#13561=ADVANCED_BREP_SHAPE_REPRESENTATION ( '', ( #15204, #2741 ), #2413 ) ;
#13584=EDGE_CURVE ( 'NONE', #5865, #11845, #20153, .T. ) ;
#13673=EDGE_CURVE ( 'NONE', #2482, #504, #11277, .T. ) ;
#13752=ORIENTED_EDGE ( 'NONE', *, *, #13673, .T. ) ;
#13881=PRODUCT_DEFINITION ( 'UNKNOWN', '', #14231, #3905 ) ;
#13917=COLOUR_RGB ( '', 0.40784314, 0.44705882, 0.49803922) ;
#14064=ORIENTED_EDGE ( 'NONE', *, *, #2016, .T. ) ;
#14102=CARTESIAN_POINT ( 'NONE',  ( 36.00000000000000000, 0.000000000000000000, -135.0000000000000284 ) ) ;
#14139=( NAMED_UNIT ( * ) PLANE_ANGLE_UNIT ( ) SI_UNIT ( $, .RADIAN. ) );
#14231=PRODUCT_DEFINITION_FORMATION_WITH_SPECIFIED_SOURCE ( 'ANY', '', #5172, .NOT_KNOWN. ) ;
#14410=ADVANCED_FACE ( 'NONE', ( #6355 ), #1678, .T. ) ;
#14531=CARTESIAN_POINT ( 'NONE',  ( 0.000000000000000000, 0.000000000000000000, -135.0000000000000284 ) ) ;
#14573=EDGE_CURVE ( 'NONE', #5865, #2482, #2097, .T. ) ;
#14587=( NAMED_UNIT ( * ) PLANE_ANGLE_UNIT ( ) SI_UNIT ( $, .RADIAN. ) );
#14644=CYLINDRICAL_SURFACE ( 'NONE', #4383, 36.00000000000000000 ) ;
#14647=MECHANICAL_DESIGN_GEOMETRIC_PRESENTATION_REPRESENTATION('',(#1450),#13021);
#15084=DIRECTION ( 'NONE',  ( 1.000000000000000000, 0.000000000000000000, 0.000000000000000000 ) ) ;
#15094=ADVANCED_FACE ( 'NONE', ( #16112 ), #19163, .T. ) ;
#15204=MANIFOLD_SOLID_BREP ( 'Boss-Extrude1', #8017 ) ;
#15545=CARTESIAN_POINT ( 'NONE',  ( 0.000000000000000000, 0.000000000000000000, -135.0000000000000284 ) ) ;
#15652=MECHANICAL_DESIGN_GEOMETRIC_PRESENTATION_REPRESENTATION('',(#3794),#19547);
#15669=VECTOR ( 'NONE', #1140, 1000.000000000000000 ) ;
#15725=( NAMED_UNIT ( * ) SI_UNIT ( $, .STERADIAN. ) SOLID_ANGLE_UNIT ( ) );
#15952=( NAMED_UNIT ( * ) SI_UNIT ( $, .STERADIAN. ) SOLID_ANGLE_UNIT ( ) );
#15970=AXIS2_PLACEMENT_3D ( 'NONE', #1940, #9110, #7172 ) ;
#16019=( NAMED_UNIT ( * ) SI_UNIT ( $, .STERADIAN. ) SOLID_ANGLE_UNIT ( ) );
#16112=FACE_OUTER_BOUND ( 'NONE', #11006, .T. ) ;
#16384=EDGE_LOOP ( 'NONE', ( #245, #17097 ) ) ;
#16677=ORIENTED_EDGE ( 'NONE', *, *, #16701, .F. ) ;
#16701=EDGE_CURVE ( 'NONE', #11845, #504, #11209, .T. ) ;
#16752=EDGE_LOOP ( 'NONE', ( #14064, #17426, #12470, #16677 ) ) ;
#16848=SURFACE_SIDE_STYLE ('',( #4364 ) ) ;
#16953=PLANE ( 'NONE',  #11345 ) ;
#17097=ORIENTED_EDGE ( 'NONE', *, *, #13584, .F. ) ;
#17342=( LENGTH_UNIT ( ) NAMED_UNIT ( * ) SI_UNIT ( .MILLI., .METRE. ) );
#17420=ORIENTED_EDGE ( 'NONE', *, *, #13584, .T. ) ;
#17426=ORIENTED_EDGE ( 'NONE', *, *, #14573, .T. ) ;
#17462=EDGE_LOOP ( 'NONE', ( #7652, #17420, #1920, #3562 ) ) ;
#17635=( LENGTH_UNIT ( ) NAMED_UNIT ( * ) SI_UNIT ( .MILLI., .METRE. ) );
#17726=FILL_AREA_STYLE ('',( #19362 ) ) ;
#17728=( NAMED_UNIT ( * ) SI_UNIT ( $, .STERADIAN. ) SOLID_ANGLE_UNIT ( ) );
#17945=UNCERTAINTY_MEASURE_WITH_UNIT (LENGTH_MEASURE( 1.000000000000000082E-05 ), #7797, 'distance_accuracy_value', 'NONE');
#17984=( NAMED_UNIT ( * ) SI_UNIT ( $, .STERADIAN. ) SOLID_ANGLE_UNIT ( ) );
#18434=ADVANCED_FACE ( 'NONE', ( #11547 ), #14644, .T. ) ;
#18470=FILL_AREA_STYLE ('',( #4787 ) ) ;
#18676=FILL_AREA_STYLE_COLOUR ( '', #3796 ) ;
#18870=FILL_AREA_STYLE ('',( #18676 ) ) ;
#19163=PLANE ( 'NONE',  #15970 ) ;
#19241=STYLED_ITEM ( 'NONE', ( #8256 ), #15094 ) ;
#19362=FILL_AREA_STYLE_COLOUR ( '', #6077 ) ;
#19532=MECHANICAL_DESIGN_GEOMETRIC_PRESENTATION_REPRESENTATION('',(#19241),#5752);
#19547=( GEOMETRIC_REPRESENTATION_CONTEXT ( 3 ) GLOBAL_UNCERTAINTY_ASSIGNED_CONTEXT ( ( #5385 ) ) GLOBAL_UNIT_ASSIGNED_CONTEXT ( ( #10755, #6328, #15725 ) ) REPRESENTATION_CONTEXT ( 'NONE', 'WORKASPACE' ) );
#19570=MECHANICAL_DESIGN_GEOMETRIC_PRESENTATION_REPRESENTATION('',(#2477),#7103);
#19728=SURFACE_STYLE_USAGE ( .BOTH. , #8257 ) ;
#19928=DIRECTION ( 'NONE',  ( 0.000000000000000000, 0.000000000000000000, 1.000000000000000000 ) ) ;
#20153=CIRCLE ( 'NONE', #10299, 36.00000000000000000 ) ;
ENDSEC;
END-ISO-10303-21;
